ISO-10303-21;
HEADER;
/* Generated by software containing ST-Developer
 * from STEP Tools, Inc. (www.steptools.com) 
 */

FILE_DESCRIPTION(
/* description */ ('Spring compression tester'),
/* implementation_level */ '2;1');

FILE_NAME(
/* name */ 'M5x25 stop screw.step',
/* time_stamp */ '2026-10-28T03:24:11-07:00',
/* author */ (''),
/* organization */ (''),
/* preprocessor_version */ 'ST-DEVELOPER v20.2',
/* originating_system */ 'Autodesk Translation Framework v15.17.0.0',
/* authorisation */ '');

FILE_SCHEMA (('AUTOMOTIVE_DESIGN { 1 0 10303 214 3 1 1 }'));
ENDSEC;

DATA;
#10=MECHANICAL_DESIGN_GEOMETRIC_PRESENTATION_REPRESENTATION('',(#1152),#43521);
#932=ORIENTED_CLOSED_SHELL('',*,#18591,.F.);
#939=BREP_WITH_VOIDS('Body1',#18590,(#932));
#958=CONICAL_SURFACE('',#20263,0.4,0.785398163397448);
#959=CONICAL_SURFACE('',#20267,0.41,0.785398163397448);
#960=CONICAL_SURFACE('',#20271,0.26,0.463647609000806);
#1017=SHAPE_REPRESENTATION_RELATIONSHIP('SRR','None',#43831,#1077);
#1077=ADVANCED_BREP_SHAPE_REPRESENTATION('',(#939),#43491);
#1152=STYLED_ITEM('',(#44209),#939);
#1468=FACE_BOUND('',#3965,.T.);
#1469=FACE_BOUND('',#3972,.T.);
#1921=PLANE('',#20255);
#1922=PLANE('',#20257);
#1923=PLANE('',#20261);
#1924=PLANE('',#20269);
#1925=PLANE('',#20274);
#1926=PLANE('',#20275);
#1927=PLANE('',#20276);
#1928=PLANE('',#20277);
#1929=PLANE('',#20278);
#1930=PLANE('',#20279);
#1931=PLANE('',#20280);
#1932=PLANE('',#20281);
#2695=FACE_OUTER_BOUND('',#3963,.T.);
#2696=FACE_OUTER_BOUND('',#3964,.T.);
#2697=FACE_OUTER_BOUND('',#3966,.T.);
#2698=FACE_OUTER_BOUND('',#3967,.T.);
#2699=FACE_OUTER_BOUND('',#3968,.T.);
#2700=FACE_OUTER_BOUND('',#3969,.T.);
#2701=FACE_OUTER_BOUND('',#3970,.T.);
#2702=FACE_OUTER_BOUND('',#3971,.T.);
#2703=FACE_OUTER_BOUND('',#3973,.T.);
#2704=FACE_OUTER_BOUND('',#3974,.T.);
#2705=FACE_OUTER_BOUND('',#3975,.T.);
#2706=FACE_OUTER_BOUND('',#3976,.T.);
#2707=FACE_OUTER_BOUND('',#3977,.T.);
#2708=FACE_OUTER_BOUND('',#3978,.T.);
#2709=FACE_OUTER_BOUND('',#3979,.T.);
#2710=FACE_OUTER_BOUND('',#3980,.T.);
#2711=FACE_OUTER_BOUND('',#3981,.T.);
#2712=FACE_OUTER_BOUND('',#3982,.T.);
#3963=EDGE_LOOP('',(#14531));
#3964=EDGE_LOOP('',(#14532));
#3965=EDGE_LOOP('',(#14533));
#3966=EDGE_LOOP('',(#14534,#14535,#14536,#14537));
#3967=EDGE_LOOP('',(#14538));
#3968=EDGE_LOOP('',(#14539,#14540,#14541,#14542));
#3969=EDGE_LOOP('',(#14543,#14544,#14545,#14546));
#3970=EDGE_LOOP('',(#14547,#14548,#14549,#14550));
#3971=EDGE_LOOP('',(#14551));
#3972=EDGE_LOOP('',(#14552));
#3973=EDGE_LOOP('',(#14553,#14554,#14555,#14556));
#3974=EDGE_LOOP('',(#14557,#14558,#14559,#14560));
#3975=EDGE_LOOP('',(#14561,#14562,#14563,#14564));
#3976=EDGE_LOOP('',(#14565,#14566,#14567,#14568));
#3977=EDGE_LOOP('',(#14569,#14570,#14571,#14572));
#3978=EDGE_LOOP('',(#14573,#14574,#14575,#14576));
#3979=EDGE_LOOP('',(#14577,#14578,#14579,#14580));
#3980=EDGE_LOOP('',(#14581,#14582,#14583,#14584));
#3981=EDGE_LOOP('',(#14585,#14586,#14587,#14588,#14589,#14590));
#3982=EDGE_LOOP('',(#14591,#14592,#14593,#14594,#14595,#14596));
#5333=LINE('',#29610,#6765);
#5334=LINE('',#29617,#6766);
#5335=LINE('',#29621,#6767);
#5336=LINE('',#29625,#6768);
#5337=LINE('',#29632,#6769);
#5338=LINE('',#29634,#6770);
#5339=LINE('',#29638,#6771);
#5340=LINE('',#29640,#6772);
#5341=LINE('',#29642,#6773);
#5342=LINE('',#29643,#6774);
#5343=LINE('',#29646,#6775);
#5344=LINE('',#29648,#6776);
#5345=LINE('',#29649,#6777);
#5346=LINE('',#29652,#6778);
#5347=LINE('',#29654,#6779);
#5348=LINE('',#29655,#6780);
#5349=LINE('',#29658,#6781);
#5350=LINE('',#29660,#6782);
#5351=LINE('',#29661,#6783);
#5352=LINE('',#29664,#6784);
#5353=LINE('',#29666,#6785);
#5354=LINE('',#29667,#6786);
#5355=LINE('',#29669,#6787);
#5356=LINE('',#29670,#6788);
#6765=VECTOR('',#23877,0.25);
#6766=VECTOR('',#23886,0.4);
#6767=VECTOR('',#23891,0.425);
#6768=VECTOR('',#23896,0.41);
#6769=VECTOR('',#23905,0.26);
#6770=VECTOR('',#23908,0.25);
#6771=VECTOR('',#23911,1.);
#6772=VECTOR('',#23912,1.);
#6773=VECTOR('',#23913,1.);
#6774=VECTOR('',#23914,1.);
#6775=VECTOR('',#23917,1.);
#6776=VECTOR('',#23918,1.);
#6777=VECTOR('',#23919,1.);
#6778=VECTOR('',#23922,1.);
#6779=VECTOR('',#23923,1.);
#6780=VECTOR('',#23924,1.);
#6781=VECTOR('',#23927,1.);
#6782=VECTOR('',#23928,1.);
#6783=VECTOR('',#23929,1.);
#6784=VECTOR('',#23932,1.);
#6785=VECTOR('',#23933,1.);
#6786=VECTOR('',#23934,1.);
#6787=VECTOR('',#23937,1.);
#6788=VECTOR('',#23938,1.);
#7868=CIRCLE('',#20256,0.25);
#7869=CIRCLE('',#20258,0.25);
#7870=CIRCLE('',#20259,0.24505);
#7871=CIRCLE('',#20262,0.375);
#7872=CIRCLE('',#20264,0.425);
#7873=CIRCLE('',#20266,0.425);
#7874=CIRCLE('',#20268,0.395);
#7875=CIRCLE('',#20270,0.27);
#7876=CIRCLE('',#20272,0.24505);
#8923=VERTEX_POINT('',#29602);
#8924=VERTEX_POINT('',#29605);
#8925=VERTEX_POINT('',#29607);
#8926=VERTEX_POINT('',#29612);
#8927=VERTEX_POINT('',#29615);
#8928=VERTEX_POINT('',#29619);
#8929=VERTEX_POINT('',#29623);
#8930=VERTEX_POINT('',#29627);
#8931=VERTEX_POINT('',#29630);
#8932=VERTEX_POINT('',#29636);
#8933=VERTEX_POINT('',#29637);
#8934=VERTEX_POINT('',#29639);
#8935=VERTEX_POINT('',#29641);
#8936=VERTEX_POINT('',#29645);
#8937=VERTEX_POINT('',#29647);
#8938=VERTEX_POINT('',#29651);
#8939=VERTEX_POINT('',#29653);
#8940=VERTEX_POINT('',#29657);
#8941=VERTEX_POINT('',#29659);
#8942=VERTEX_POINT('',#29663);
#8943=VERTEX_POINT('',#29665);
#10930=EDGE_CURVE('',#8923,#8923,#7868,.T.);
#10931=EDGE_CURVE('',#8924,#8924,#7869,.T.);
#10932=EDGE_CURVE('',#8925,#8925,#7870,.T.);
#10933=EDGE_CURVE('',#8924,#8923,#5333,.T.);
#10934=EDGE_CURVE('',#8926,#8926,#7871,.T.);
#10935=EDGE_CURVE('',#8927,#8927,#7872,.T.);
#10936=EDGE_CURVE('',#8927,#8926,#5334,.T.);
#10937=EDGE_CURVE('',#8928,#8928,#7873,.T.);
#10938=EDGE_CURVE('',#8928,#8927,#5335,.T.);
#10939=EDGE_CURVE('',#8929,#8929,#7874,.T.);
#10940=EDGE_CURVE('',#8929,#8928,#5336,.T.);
#10941=EDGE_CURVE('',#8930,#8930,#7875,.T.);
#10942=EDGE_CURVE('',#8931,#8931,#7876,.F.);
#10943=EDGE_CURVE('',#8931,#8930,#5337,.T.);
#10944=EDGE_CURVE('',#8925,#8931,#5338,.T.);
#10945=EDGE_CURVE('',#8932,#8933,#5339,.T.);
#10946=EDGE_CURVE('',#8933,#8934,#5340,.T.);
#10947=EDGE_CURVE('',#8934,#8935,#5341,.T.);
#10948=EDGE_CURVE('',#8932,#8935,#5342,.T.);
#10949=EDGE_CURVE('',#8933,#8936,#5343,.T.);
#10950=EDGE_CURVE('',#8936,#8937,#5344,.T.);
#10951=EDGE_CURVE('',#8937,#8934,#5345,.T.);
#10952=EDGE_CURVE('',#8936,#8938,#5346,.T.);
#10953=EDGE_CURVE('',#8938,#8939,#5347,.T.);
#10954=EDGE_CURVE('',#8939,#8937,#5348,.T.);
#10955=EDGE_CURVE('',#8938,#8940,#5349,.T.);
#10956=EDGE_CURVE('',#8940,#8941,#5350,.T.);
#10957=EDGE_CURVE('',#8941,#8939,#5351,.T.);
#10958=EDGE_CURVE('',#8940,#8942,#5352,.T.);
#10959=EDGE_CURVE('',#8942,#8943,#5353,.T.);
#10960=EDGE_CURVE('',#8943,#8941,#5354,.T.);
#10961=EDGE_CURVE('',#8942,#8932,#5355,.T.);
#10962=EDGE_CURVE('',#8935,#8943,#5356,.T.);
#14531=ORIENTED_EDGE('',*,*,#10930,.F.);
#14532=ORIENTED_EDGE('',*,*,#10931,.T.);
#14533=ORIENTED_EDGE('',*,*,#10932,.F.);
#14534=ORIENTED_EDGE('',*,*,#10931,.F.);
#14535=ORIENTED_EDGE('',*,*,#10933,.T.);
#14536=ORIENTED_EDGE('',*,*,#10930,.T.);
#14537=ORIENTED_EDGE('',*,*,#10933,.F.);
#14538=ORIENTED_EDGE('',*,*,#10934,.F.);
#14539=ORIENTED_EDGE('',*,*,#10935,.F.);
#14540=ORIENTED_EDGE('',*,*,#10936,.T.);
#14541=ORIENTED_EDGE('',*,*,#10934,.T.);
#14542=ORIENTED_EDGE('',*,*,#10936,.F.);
#14543=ORIENTED_EDGE('',*,*,#10937,.F.);
#14544=ORIENTED_EDGE('',*,*,#10938,.T.);
#14545=ORIENTED_EDGE('',*,*,#10935,.T.);
#14546=ORIENTED_EDGE('',*,*,#10938,.F.);
#14547=ORIENTED_EDGE('',*,*,#10939,.F.);
#14548=ORIENTED_EDGE('',*,*,#10940,.T.);
#14549=ORIENTED_EDGE('',*,*,#10937,.T.);
#14550=ORIENTED_EDGE('',*,*,#10940,.F.);
#14551=ORIENTED_EDGE('',*,*,#10939,.T.);
#14552=ORIENTED_EDGE('',*,*,#10941,.F.);
#14553=ORIENTED_EDGE('',*,*,#10942,.F.);
#14554=ORIENTED_EDGE('',*,*,#10943,.T.);
#14555=ORIENTED_EDGE('',*,*,#10941,.T.);
#14556=ORIENTED_EDGE('',*,*,#10943,.F.);
#14557=ORIENTED_EDGE('',*,*,#10932,.T.);
#14558=ORIENTED_EDGE('',*,*,#10944,.T.);
#14559=ORIENTED_EDGE('',*,*,#10942,.T.);
#14560=ORIENTED_EDGE('',*,*,#10944,.F.);
#14561=ORIENTED_EDGE('',*,*,#10945,.T.);
#14562=ORIENTED_EDGE('',*,*,#10946,.T.);
#14563=ORIENTED_EDGE('',*,*,#10947,.T.);
#14564=ORIENTED_EDGE('',*,*,#10948,.F.);
#14565=ORIENTED_EDGE('',*,*,#10949,.T.);
#14566=ORIENTED_EDGE('',*,*,#10950,.T.);
#14567=ORIENTED_EDGE('',*,*,#10951,.T.);
#14568=ORIENTED_EDGE('',*,*,#10946,.F.);
#14569=ORIENTED_EDGE('',*,*,#10952,.T.);
#14570=ORIENTED_EDGE('',*,*,#10953,.T.);
#14571=ORIENTED_EDGE('',*,*,#10954,.T.);
#14572=ORIENTED_EDGE('',*,*,#10950,.F.);
#14573=ORIENTED_EDGE('',*,*,#10955,.T.);
#14574=ORIENTED_EDGE('',*,*,#10956,.T.);
#14575=ORIENTED_EDGE('',*,*,#10957,.T.);
#14576=ORIENTED_EDGE('',*,*,#10953,.F.);
#14577=ORIENTED_EDGE('',*,*,#10958,.T.);
#14578=ORIENTED_EDGE('',*,*,#10959,.T.);
#14579=ORIENTED_EDGE('',*,*,#10960,.T.);
#14580=ORIENTED_EDGE('',*,*,#10956,.F.);
#14581=ORIENTED_EDGE('',*,*,#10961,.T.);
#14582=ORIENTED_EDGE('',*,*,#10948,.T.);
#14583=ORIENTED_EDGE('',*,*,#10962,.T.);
#14584=ORIENTED_EDGE('',*,*,#10959,.F.);
#14585=ORIENTED_EDGE('',*,*,#10961,.F.);
#14586=ORIENTED_EDGE('',*,*,#10958,.F.);
#14587=ORIENTED_EDGE('',*,*,#10955,.F.);
#14588=ORIENTED_EDGE('',*,*,#10952,.F.);
#14589=ORIENTED_EDGE('',*,*,#10949,.F.);
#14590=ORIENTED_EDGE('',*,*,#10945,.F.);
#14591=ORIENTED_EDGE('',*,*,#10962,.F.);
#14592=ORIENTED_EDGE('',*,*,#10947,.F.);
#14593=ORIENTED_EDGE('',*,*,#10951,.F.);
#14594=ORIENTED_EDGE('',*,*,#10954,.F.);
#14595=ORIENTED_EDGE('',*,*,#10957,.F.);
#14596=ORIENTED_EDGE('',*,*,#10960,.F.);
#17251=CYLINDRICAL_SURFACE('',#20260,0.25);
#17252=CYLINDRICAL_SURFACE('',#20265,0.425);
#17253=CYLINDRICAL_SURFACE('',#20273,0.24505);
#18019=ADVANCED_FACE('',(#2695),#1921,.F.);
#18020=ADVANCED_FACE('',(#2696,#1468),#1922,.T.);
#18021=ADVANCED_FACE('',(#2697),#17251,.T.);
#18022=ADVANCED_FACE('',(#2698),#1923,.T.);
#18023=ADVANCED_FACE('',(#2699),#958,.T.);
#18024=ADVANCED_FACE('',(#2700),#17252,.T.);
#18025=ADVANCED_FACE('',(#2701),#959,.T.);
#18026=ADVANCED_FACE('',(#2702,#1469),#1924,.T.);
#18027=ADVANCED_FACE('',(#2703),#960,.T.);
#18028=ADVANCED_FACE('',(#2704),#17253,.T.);
#18029=ADVANCED_FACE('',(#2705),#1925,.F.);
#18030=ADVANCED_FACE('',(#2706),#1926,.F.);
#18031=ADVANCED_FACE('',(#2707),#1927,.F.);
#18032=ADVANCED_FACE('',(#2708),#1928,.F.);
#18033=ADVANCED_FACE('',(#2709),#1929,.F.);
#18034=ADVANCED_FACE('',(#2710),#1930,.F.);
#18035=ADVANCED_FACE('',(#2711),#1931,.F.);
#18036=ADVANCED_FACE('',(#2712),#1932,.F.);
#18590=CLOSED_SHELL('',(#18019,#18020,#18021,#18022,#18023,#18024,#18025,
#18026,#18027,#18028));
#18591=CLOSED_SHELL('',(#18029,#18030,#18031,#18032,#18033,#18034,#18035,
#18036));
#20254=AXIS2_PLACEMENT_3D('',#29600,#23863,#23864);
#20255=AXIS2_PLACEMENT_3D('',#29601,#23865,#23866);
#20256=AXIS2_PLACEMENT_3D('',#29603,#23867,#23868);
#20257=AXIS2_PLACEMENT_3D('',#29604,#23869,#23870);
#20258=AXIS2_PLACEMENT_3D('',#29606,#23871,#23872);
#20259=AXIS2_PLACEMENT_3D('',#29608,#23873,#23874);
#20260=AXIS2_PLACEMENT_3D('',#29609,#23875,#23876);
#20261=AXIS2_PLACEMENT_3D('',#29611,#23878,#23879);
#20262=AXIS2_PLACEMENT_3D('',#29613,#23880,#23881);
#20263=AXIS2_PLACEMENT_3D('',#29614,#23882,#23883);
#20264=AXIS2_PLACEMENT_3D('',#29616,#23884,#23885);
#20265=AXIS2_PLACEMENT_3D('',#29618,#23887,#23888);
#20266=AXIS2_PLACEMENT_3D('',#29620,#23889,#23890);
#20267=AXIS2_PLACEMENT_3D('',#29622,#23892,#23893);
#20268=AXIS2_PLACEMENT_3D('',#29624,#23894,#23895);
#20269=AXIS2_PLACEMENT_3D('',#29626,#23897,#23898);
#20270=AXIS2_PLACEMENT_3D('',#29628,#23899,#23900);
#20271=AXIS2_PLACEMENT_3D('',#29629,#23901,#23902);
#20272=AXIS2_PLACEMENT_3D('',#29631,#23903,#23904);
#20273=AXIS2_PLACEMENT_3D('',#29633,#23906,#23907);
#20274=AXIS2_PLACEMENT_3D('',#29635,#23909,#23910);
#20275=AXIS2_PLACEMENT_3D('',#29644,#23915,#23916);
#20276=AXIS2_PLACEMENT_3D('',#29650,#23920,#23921);
#20277=AXIS2_PLACEMENT_3D('',#29656,#23925,#23926);
#20278=AXIS2_PLACEMENT_3D('',#29662,#23930,#23931);
#20279=AXIS2_PLACEMENT_3D('',#29668,#23935,#23936);
#20280=AXIS2_PLACEMENT_3D('',#29671,#23939,#23940);
#20281=AXIS2_PLACEMENT_3D('',#29672,#23941,#23942);
#23863=DIRECTION('axis',(0.,0.,1.));
#23864=DIRECTION('refdir',(1.,0.,0.));
#23865=DIRECTION('center_axis',(0.,1.,0.));
#23866=DIRECTION('ref_axis',(1.,0.,0.));
#23867=DIRECTION('center_axis',(0.,1.,0.));
#23868=DIRECTION('ref_axis',(1.,0.,0.));
#23869=DIRECTION('center_axis',(0.,1.,0.));
#23870=DIRECTION('ref_axis',(1.,0.,0.));
#23871=DIRECTION('center_axis',(0.,1.,0.));
#23872=DIRECTION('ref_axis',(1.,0.,0.));
#23873=DIRECTION('center_axis',(0.,1.,0.));
#23874=DIRECTION('ref_axis',(1.,0.,0.));
#23875=DIRECTION('center_axis',(0.,1.,0.));
#23876=DIRECTION('ref_axis',(1.,0.,0.));
#23877=DIRECTION('',(0.,-1.,0.));
#23878=DIRECTION('center_axis',(0.,1.,0.));
#23879=DIRECTION('ref_axis',(0.,0.,1.));
#23880=DIRECTION('center_axis',(0.,-1.,0.));
#23881=DIRECTION('ref_axis',(1.,0.,0.));
#23882=DIRECTION('center_axis',(0.,-1.,0.));
#23883=DIRECTION('ref_axis',(1.,0.,0.));
#23884=DIRECTION('center_axis',(0.,-1.,0.));
#23885=DIRECTION('ref_axis',(1.,0.,0.));
#23886=DIRECTION('',(0.707106781186548,0.707106781186547,8.65956056235493E-17));
#23887=DIRECTION('center_axis',(0.,-1.,0.));
#23888=DIRECTION('ref_axis',(1.,0.,0.));
#23889=DIRECTION('center_axis',(0.,-1.,0.));
#23890=DIRECTION('ref_axis',(1.,0.,0.));
#23891=DIRECTION('',(0.,1.,0.));
#23892=DIRECTION('center_axis',(0.,1.,0.));
#23893=DIRECTION('ref_axis',(1.,0.,0.));
#23894=DIRECTION('center_axis',(0.,-1.,0.));
#23895=DIRECTION('ref_axis',(1.,0.,0.));
#23896=DIRECTION('',(-0.707106781186547,0.707106781186548,-8.65956056235493E-17));
#23897=DIRECTION('center_axis',(0.,-1.,0.));
#23898=DIRECTION('ref_axis',(0.,0.,-1.));
#23899=DIRECTION('center_axis',(0.,-1.,0.));
#23900=DIRECTION('ref_axis',(1.,0.,0.));
#23901=DIRECTION('center_axis',(0.,1.,0.));
#23902=DIRECTION('ref_axis',(1.,0.,0.));
#23903=DIRECTION('center_axis',(0.,1.,0.));
#23904=DIRECTION('ref_axis',(1.,0.,0.));
#23905=DIRECTION('',(-0.447213595499958,0.894427190999916,-5.47678698264203E-17));
#23906=DIRECTION('center_axis',(0.,-1.,0.));
#23907=DIRECTION('ref_axis',(1.,0.,0.));
#23908=DIRECTION('',(0.,1.,0.));
#23909=DIRECTION('center_axis',(0.866025403784439,0.,-0.5));
#23910=DIRECTION('ref_axis',(0.5,0.,0.866025403784439));
#23911=DIRECTION('',(-0.5,0.,-0.866025403784439));
#23912=DIRECTION('',(0.,-1.,0.));
#23913=DIRECTION('',(0.5,0.,0.866025403784439));
#23914=DIRECTION('',(0.,-1.,0.));
#23915=DIRECTION('center_axis',(1.20185167898973E-16,0.,-1.));
#23916=DIRECTION('ref_axis',(1.,0.,1.20185167898973E-16));
#23917=DIRECTION('',(-1.,0.,-1.20185167898973E-16));
#23918=DIRECTION('',(0.,-1.,0.));
#23919=DIRECTION('',(1.,0.,1.20185167898973E-16));
#23920=DIRECTION('center_axis',(-0.866025403784439,0.,-0.5));
#23921=DIRECTION('ref_axis',(0.5,0.,-0.866025403784439));
#23922=DIRECTION('',(-0.5,0.,0.866025403784439));
#23923=DIRECTION('',(0.,-1.,0.));
#23924=DIRECTION('',(0.5,0.,-0.866025403784439));
#23925=DIRECTION('center_axis',(-0.866025403784439,0.,0.5));
#23926=DIRECTION('ref_axis',(-0.5,0.,-0.866025403784439));
#23927=DIRECTION('',(0.5,0.,0.866025403784439));
#23928=DIRECTION('',(0.,-1.,0.));
#23929=DIRECTION('',(-0.5,0.,-0.866025403784439));
#23930=DIRECTION('center_axis',(-2.40370335797945E-16,0.,1.));
#23931=DIRECTION('ref_axis',(-1.,0.,-2.40370335797945E-16));
#23932=DIRECTION('',(1.,0.,2.40370335797945E-16));
#23933=DIRECTION('',(0.,-1.,0.));
#23934=DIRECTION('',(-1.,0.,-2.40370335797945E-16));
#23935=DIRECTION('center_axis',(0.866025403784439,0.,0.5));
#23936=DIRECTION('ref_axis',(-0.5,0.,0.866025403784439));
#23937=DIRECTION('',(0.5,0.,-0.866025403784439));
#23938=DIRECTION('',(-0.5,0.,0.866025403784439));
#23939=DIRECTION('center_axis',(0.,1.,0.));
#23940=DIRECTION('ref_axis',(1.,0.,0.));
#23941=DIRECTION('center_axis',(0.,-1.,0.));
#23942=DIRECTION('ref_axis',(0.,0.,-1.));
#29600=CARTESIAN_POINT('',(0.,0.,0.));
#29601=CARTESIAN_POINT('Origin',(0.,-2.5,0.));
#29602=CARTESIAN_POINT('',(-0.25,-2.5,3.06161699786838E-17));
#29603=CARTESIAN_POINT('Origin',(0.,-2.5,0.));
#29604=CARTESIAN_POINT('Origin',(0.,-1.9,0.));
#29605=CARTESIAN_POINT('',(-0.25,-1.9,3.06161699786838E-17));
#29606=CARTESIAN_POINT('Origin',(0.,-1.9,0.));
#29607=CARTESIAN_POINT('',(-0.24505,-1.9,3.00099698131059E-17));
#29608=CARTESIAN_POINT('Origin',(0.,-1.9,0.));
#29609=CARTESIAN_POINT('Origin',(0.,-3.,0.));
#29610=CARTESIAN_POINT('',(-0.25,-3.,3.06161699786838E-17));
#29611=CARTESIAN_POINT('Origin',(0.375,0.5,0.));
#29612=CARTESIAN_POINT('',(-0.375,0.5,-4.59242549680257E-17));
#29613=CARTESIAN_POINT('Origin',(0.,0.5,0.));
#29614=CARTESIAN_POINT('Origin',(0.,0.475,0.));
#29615=CARTESIAN_POINT('',(-0.425,0.45,-5.20474889637625E-17));
#29616=CARTESIAN_POINT('Origin',(0.,0.45,0.));
#29617=CARTESIAN_POINT('',(-0.4,0.475,-4.89858719658941E-17));
#29618=CARTESIAN_POINT('Origin',(0.,0.24,0.));
#29619=CARTESIAN_POINT('',(-0.425,0.0299999999999998,-5.20474889637625E-17));
#29620=CARTESIAN_POINT('Origin',(0.,0.0299999999999998,0.));
#29621=CARTESIAN_POINT('',(-0.425,0.24,-5.20474889637625E-17));
#29622=CARTESIAN_POINT('Origin',(0.,0.0150000000000001,0.));
#29623=CARTESIAN_POINT('',(-0.395,4.85722573273506E-17,-4.83735485663204E-17));
#29624=CARTESIAN_POINT('Origin',(0.,0.,0.));
#29625=CARTESIAN_POINT('',(-0.41,0.0150000000000001,-5.02105187650415E-17));
#29626=CARTESIAN_POINT('Origin',(0.27,0.,0.));
#29627=CARTESIAN_POINT('',(-0.27,0.,-3.30654635769785E-17));
#29628=CARTESIAN_POINT('Origin',(0.,0.,0.));
#29629=CARTESIAN_POINT('Origin',(0.,-0.02,0.));
#29630=CARTESIAN_POINT('',(-0.24505,-0.0498999999999999,3.00099698131059E-17));
#29631=CARTESIAN_POINT('Origin',(0.,-0.0498999999999999,0.));
#29632=CARTESIAN_POINT('',(-0.26,-0.02,-3.18408167778312E-17));
#29633=CARTESIAN_POINT('Origin',(0.,-0.995,0.));
#29634=CARTESIAN_POINT('',(-0.24505,-0.995,-3.00099698131059E-17));
#29635=CARTESIAN_POINT('Origin',(0.115470053837925,-0.5,-0.2));
#29636=CARTESIAN_POINT('',(0.23094010767585,-0.5,0.));
#29637=CARTESIAN_POINT('',(0.115470053837925,-0.5,-0.2));
#29638=CARTESIAN_POINT('',(0.23094010767585,-0.5,0.));
#29639=CARTESIAN_POINT('',(0.115470053837925,-0.8,-0.2));
#29640=CARTESIAN_POINT('',(0.115470053837925,-0.5,-0.2));
#29641=CARTESIAN_POINT('',(0.23094010767585,-0.8,0.));
#29642=CARTESIAN_POINT('',(0.23094010767585,-0.8,0.));
#29643=CARTESIAN_POINT('',(0.23094010767585,-0.5,0.));
#29644=CARTESIAN_POINT('Origin',(-0.115470053837925,-0.5,-0.2));
#29645=CARTESIAN_POINT('',(-0.115470053837925,-0.5,-0.2));
#29646=CARTESIAN_POINT('',(0.115470053837925,-0.5,-0.2));
#29647=CARTESIAN_POINT('',(-0.115470053837925,-0.8,-0.2));
#29648=CARTESIAN_POINT('',(-0.115470053837925,-0.5,-0.2));
#29649=CARTESIAN_POINT('',(0.115470053837925,-0.8,-0.2));
#29650=CARTESIAN_POINT('Origin',(-0.23094010767585,-0.5,-2.77555756156289E-17));
#29651=CARTESIAN_POINT('',(-0.23094010767585,-0.5,-2.82820063659975E-17));
#29652=CARTESIAN_POINT('',(-0.115470053837925,-0.5,-0.2));
#29653=CARTESIAN_POINT('',(-0.23094010767585,-0.8,-2.77555756156289E-17));
#29654=CARTESIAN_POINT('',(-0.23094010767585,-0.5,-2.82820063659975E-17));
#29655=CARTESIAN_POINT('',(-0.115470053837925,-0.8,-0.2));
#29656=CARTESIAN_POINT('Origin',(-0.115470053837925,-0.5,0.2));
#29657=CARTESIAN_POINT('',(-0.115470053837925,-0.5,0.2));
#29658=CARTESIAN_POINT('',(-0.23094010767585,-0.5,-2.82820063659975E-17));
#29659=CARTESIAN_POINT('',(-0.115470053837925,-0.8,0.2));
#29660=CARTESIAN_POINT('',(-0.115470053837925,-0.5,0.2));
#29661=CARTESIAN_POINT('',(-0.23094010767585,-0.8,-2.82820063659975E-17));
#29662=CARTESIAN_POINT('Origin',(0.115470053837925,-0.5,0.2));
#29663=CARTESIAN_POINT('',(0.115470053837925,-0.5,0.2));
#29664=CARTESIAN_POINT('',(-0.115470053837925,-0.5,0.2));
#29665=CARTESIAN_POINT('',(0.115470053837925,-0.8,0.2));
#29666=CARTESIAN_POINT('',(0.115470053837925,-0.5,0.2));
#29667=CARTESIAN_POINT('',(-0.115470053837925,-0.8,0.2));
#29668=CARTESIAN_POINT('Origin',(0.23094010767585,-0.5,0.));
#29669=CARTESIAN_POINT('',(0.115470053837925,-0.5,0.2));
#29670=CARTESIAN_POINT('',(0.115470053837925,-0.8,0.2));
#29671=CARTESIAN_POINT('Origin',(0.,-0.5,0.));
#29672=CARTESIAN_POINT('Origin',(0.,-0.8,0.));
#43423=UNCERTAINTY_MEASURE_WITH_UNIT(LENGTH_MEASURE(0.001),#43522,
'DISTANCE_ACCURACY_VALUE',
'Maximum model space distance between geometric entities at asserted c
onnectivities');
#43453=UNCERTAINTY_MEASURE_WITH_UNIT(LENGTH_MEASURE(0.001),#43522,
'DISTANCE_ACCURACY_VALUE',
'Maximum model space distance between geometric entities at asserted c
onnectivities');
#43491=(
GEOMETRIC_REPRESENTATION_CONTEXT(3)
GLOBAL_UNCERTAINTY_ASSIGNED_CONTEXT((#43423))
GLOBAL_UNIT_ASSIGNED_CONTEXT((#43522,#43524,#43525))
REPRESENTATION_CONTEXT('','3D')
);
#43521=(
GEOMETRIC_REPRESENTATION_CONTEXT(3)
GLOBAL_UNCERTAINTY_ASSIGNED_CONTEXT((#43453))
GLOBAL_UNIT_ASSIGNED_CONTEXT((#43522,#43524,#43525))
REPRESENTATION_CONTEXT('','3D')
);
#43522=(
LENGTH_UNIT()
NAMED_UNIT(*)
SI_UNIT(.CENTI.,.METRE.)
);
#43524=(
NAMED_UNIT(*)
PLANE_ANGLE_UNIT()
SI_UNIT($,.RADIAN.)
);
#43525=(
NAMED_UNIT(*)
SI_UNIT($,.STERADIAN.)
SOLID_ANGLE_UNIT()
);
#43563=SHAPE_DEFINITION_REPRESENTATION(#43640,#43831);
#43640=PRODUCT_DEFINITION_SHAPE('',$,#43899);
#43831=SHAPE_REPRESENTATION('',(#20254),#43491);
#43861=PRODUCT_DEFINITION_CONTEXT('part definition',#44064,'design');
#43899=PRODUCT_DEFINITION('M5x25 stop screw','M5x25 stop screw',#43966,
#43861);
#43966=PRODUCT_DEFINITION_FORMATION('',$,#44103);
#44064=APPLICATION_CONTEXT(
'Core Data for Automotive Mechanical Design Process');
#44065=PRODUCT_CONTEXT('part definition',#44064,'mechanical');
#44103=PRODUCT('M5x25 stop screw','M5x25 stop screw','M5x25 stop screw',
(#44065));
#44203=COLOUR_RGB('Black',0.12,0.14,0.17);
#44204=FILL_AREA_STYLE_COLOUR('',#44203);
#44205=FILL_AREA_STYLE('',(#44204));
#44206=SURFACE_STYLE_FILL_AREA(#44205);
#44207=SURFACE_SIDE_STYLE('',(#44206));
#44208=SURFACE_STYLE_USAGE(.BOTH.,#44207);
#44209=PRESENTATION_STYLE_ASSIGNMENT((#44208));
ENDSEC;
END-ISO-10303-21;
